ISO-10303-21;
HEADER;
/* Generated by software containing ST-Developer
 * from STEP Tools, Inc. (www.steptools.com) 
 */

FILE_DESCRIPTION(
/* description */ ('Cam-and-follower valve demonstrator'),
/* implementation_level */ '2;1');

FILE_NAME(
/* name */ 'Bearing cap (3).step',
/* time_stamp */ '2026-10-28T03:25:17-07:00',
/* author */ (''),
/* organization */ (''),
/* preprocessor_version */ 'ST-DEVELOPER v20.2',
/* originating_system */ 'Autodesk Translation Framework v15.17.0.0',
/* authorisation */ '');

FILE_SCHEMA (('AUTOMOTIVE_DESIGN { 1 0 10303 214 3 1 1 }'));
ENDSEC;

DATA;
#10=MECHANICAL_DESIGN_GEOMETRIC_PRESENTATION_REPRESENTATION('',(#420),#12896);
#348=SHAPE_REPRESENTATION_RELATIONSHIP('SRR','None',#13064,#384);
#384=ADVANCED_BREP_SHAPE_REPRESENTATION('',(#463),#12864);
#420=STYLED_ITEM('',(#13330),#463);
#463=MANIFOLD_SOLID_BREP('Body1',#6187);
#569=FACE_BOUND('',#1636,.T.);
#570=FACE_BOUND('',#1640,.T.);
#571=FACE_BOUND('',#1641,.T.);
#572=FACE_BOUND('',#1642,.T.);
#573=FACE_BOUND('',#1643,.T.);
#574=FACE_BOUND('',#1644,.T.);
#575=FACE_BOUND('',#1646,.T.);
#576=FACE_BOUND('',#1647,.T.);
#577=FACE_BOUND('',#1648,.T.);
#578=FACE_BOUND('',#1649,.T.);
#579=FACE_BOUND('',#1650,.T.);
#741=CIRCLE('',#6809,0.225);
#742=CIRCLE('',#6810,0.225);
#743=CIRCLE('',#6812,0.225);
#744=CIRCLE('',#6813,0.225);
#745=CIRCLE('',#6815,0.225);
#746=CIRCLE('',#6816,0.225);
#747=CIRCLE('',#6818,0.225);
#748=CIRCLE('',#6819,0.225);
#749=CIRCLE('',#6821,1.59);
#750=CIRCLE('',#6822,1.59);
#751=CIRCLE('',#6824,1.005);
#752=CIRCLE('',#6826,1.005);
#753=CIRCLE('',#6828,2.4);
#754=CIRCLE('',#6829,2.4);
#1014=CYLINDRICAL_SURFACE('',#6808,0.225);
#1015=CYLINDRICAL_SURFACE('',#6811,0.225);
#1016=CYLINDRICAL_SURFACE('',#6814,0.225);
#1017=CYLINDRICAL_SURFACE('',#6817,0.225);
#1018=CYLINDRICAL_SURFACE('',#6820,1.59);
#1019=CYLINDRICAL_SURFACE('',#6825,1.005);
#1020=CYLINDRICAL_SURFACE('',#6827,2.4);
#1188=FACE_OUTER_BOUND('',#1630,.T.);
#1189=FACE_OUTER_BOUND('',#1631,.T.);
#1190=FACE_OUTER_BOUND('',#1632,.T.);
#1191=FACE_OUTER_BOUND('',#1633,.T.);
#1192=FACE_OUTER_BOUND('',#1634,.T.);
#1193=FACE_OUTER_BOUND('',#1635,.T.);
#1194=FACE_OUTER_BOUND('',#1637,.T.);
#1195=FACE_OUTER_BOUND('',#1638,.T.);
#1196=FACE_OUTER_BOUND('',#1639,.T.);
#1197=FACE_OUTER_BOUND('',#1645,.T.);
#1630=EDGE_LOOP('',(#4533,#4534,#4535,#4536));
#1631=EDGE_LOOP('',(#4537,#4538,#4539,#4540));
#1632=EDGE_LOOP('',(#4541,#4542,#4543,#4544));
#1633=EDGE_LOOP('',(#4545,#4546,#4547,#4548));
#1634=EDGE_LOOP('',(#4549,#4550,#4551,#4552));
#1635=EDGE_LOOP('',(#4553));
#1636=EDGE_LOOP('',(#4554));
#1637=EDGE_LOOP('',(#4555,#4556,#4557,#4558));
#1638=EDGE_LOOP('',(#4559,#4560,#4561,#4562));
#1639=EDGE_LOOP('',(#4563));
#1640=EDGE_LOOP('',(#4564));
#1641=EDGE_LOOP('',(#4565));
#1642=EDGE_LOOP('',(#4566));
#1643=EDGE_LOOP('',(#4567));
#1644=EDGE_LOOP('',(#4568));
#1645=EDGE_LOOP('',(#4569));
#1646=EDGE_LOOP('',(#4570));
#1647=EDGE_LOOP('',(#4571));
#1648=EDGE_LOOP('',(#4572));
#1649=EDGE_LOOP('',(#4573));
#1650=EDGE_LOOP('',(#4574));
#2132=LINE('',#9893,#2554);
#2133=LINE('',#9899,#2555);
#2134=LINE('',#9905,#2556);
#2135=LINE('',#9911,#2557);
#2136=LINE('',#9917,#2558);
#2137=LINE('',#9925,#2559);
#2138=LINE('',#9930,#2560);
#2554=VECTOR('',#7927,0.225);
#2555=VECTOR('',#7934,0.225);
#2556=VECTOR('',#7941,0.225);
#2557=VECTOR('',#7948,0.225);
#2558=VECTOR('',#7955,1.59);
#2559=VECTOR('',#7966,1.005);
#2560=VECTOR('',#7971,2.4);
#2985=VERTEX_POINT('',#9890);
#2986=VERTEX_POINT('',#9892);
#2987=VERTEX_POINT('',#9896);
#2988=VERTEX_POINT('',#9898);
#2989=VERTEX_POINT('',#9902);
#2990=VERTEX_POINT('',#9904);
#2991=VERTEX_POINT('',#9908);
#2992=VERTEX_POINT('',#9910);
#2993=VERTEX_POINT('',#9914);
#2994=VERTEX_POINT('',#9916);
#2995=VERTEX_POINT('',#9920);
#2996=VERTEX_POINT('',#9923);
#2997=VERTEX_POINT('',#9927);
#2998=VERTEX_POINT('',#9929);
#3563=EDGE_CURVE('',#2985,#2985,#741,.T.);
#3564=EDGE_CURVE('',#2985,#2986,#2132,.T.);
#3565=EDGE_CURVE('',#2986,#2986,#742,.T.);
#3566=EDGE_CURVE('',#2987,#2987,#743,.T.);
#3567=EDGE_CURVE('',#2987,#2988,#2133,.T.);
#3568=EDGE_CURVE('',#2988,#2988,#744,.T.);
#3569=EDGE_CURVE('',#2989,#2989,#745,.T.);
#3570=EDGE_CURVE('',#2989,#2990,#2134,.T.);
#3571=EDGE_CURVE('',#2990,#2990,#746,.T.);
#3572=EDGE_CURVE('',#2991,#2991,#747,.T.);
#3573=EDGE_CURVE('',#2991,#2992,#2135,.T.);
#3574=EDGE_CURVE('',#2992,#2992,#748,.T.);
#3575=EDGE_CURVE('',#2993,#2993,#749,.T.);
#3576=EDGE_CURVE('',#2993,#2994,#2136,.T.);
#3577=EDGE_CURVE('',#2994,#2994,#750,.T.);
#3578=EDGE_CURVE('',#2995,#2995,#751,.T.);
#3579=EDGE_CURVE('',#2996,#2996,#752,.T.);
#3580=EDGE_CURVE('',#2996,#2995,#2137,.T.);
#3581=EDGE_CURVE('',#2997,#2997,#753,.T.);
#3582=EDGE_CURVE('',#2997,#2998,#2138,.T.);
#3583=EDGE_CURVE('',#2998,#2998,#754,.T.);
#4533=ORIENTED_EDGE('',*,*,#3563,.F.);
#4534=ORIENTED_EDGE('',*,*,#3564,.T.);
#4535=ORIENTED_EDGE('',*,*,#3565,.F.);
#4536=ORIENTED_EDGE('',*,*,#3564,.F.);
#4537=ORIENTED_EDGE('',*,*,#3566,.F.);
#4538=ORIENTED_EDGE('',*,*,#3567,.T.);
#4539=ORIENTED_EDGE('',*,*,#3568,.F.);
#4540=ORIENTED_EDGE('',*,*,#3567,.F.);
#4541=ORIENTED_EDGE('',*,*,#3569,.F.);
#4542=ORIENTED_EDGE('',*,*,#3570,.T.);
#4543=ORIENTED_EDGE('',*,*,#3571,.F.);
#4544=ORIENTED_EDGE('',*,*,#3570,.F.);
#4545=ORIENTED_EDGE('',*,*,#3572,.F.);
#4546=ORIENTED_EDGE('',*,*,#3573,.T.);
#4547=ORIENTED_EDGE('',*,*,#3574,.F.);
#4548=ORIENTED_EDGE('',*,*,#3573,.F.);
#4549=ORIENTED_EDGE('',*,*,#3575,.F.);
#4550=ORIENTED_EDGE('',*,*,#3576,.T.);
#4551=ORIENTED_EDGE('',*,*,#3577,.T.);
#4552=ORIENTED_EDGE('',*,*,#3576,.F.);
#4553=ORIENTED_EDGE('',*,*,#3577,.F.);
#4554=ORIENTED_EDGE('',*,*,#3578,.F.);
#4555=ORIENTED_EDGE('',*,*,#3579,.F.);
#4556=ORIENTED_EDGE('',*,*,#3580,.T.);
#4557=ORIENTED_EDGE('',*,*,#3578,.T.);
#4558=ORIENTED_EDGE('',*,*,#3580,.F.);
#4559=ORIENTED_EDGE('',*,*,#3581,.F.);
#4560=ORIENTED_EDGE('',*,*,#3582,.T.);
#4561=ORIENTED_EDGE('',*,*,#3583,.T.);
#4562=ORIENTED_EDGE('',*,*,#3582,.F.);
#4563=ORIENTED_EDGE('',*,*,#3581,.T.);
#4564=ORIENTED_EDGE('',*,*,#3579,.T.);
#4565=ORIENTED_EDGE('',*,*,#3574,.T.);
#4566=ORIENTED_EDGE('',*,*,#3571,.T.);
#4567=ORIENTED_EDGE('',*,*,#3568,.T.);
#4568=ORIENTED_EDGE('',*,*,#3565,.T.);
#4569=ORIENTED_EDGE('',*,*,#3583,.F.);
#4570=ORIENTED_EDGE('',*,*,#3575,.T.);
#4571=ORIENTED_EDGE('',*,*,#3572,.T.);
#4572=ORIENTED_EDGE('',*,*,#3569,.T.);
#4573=ORIENTED_EDGE('',*,*,#3566,.T.);
#4574=ORIENTED_EDGE('',*,*,#3563,.T.);
#5649=PLANE('',#6823);
#5650=PLANE('',#6830);
#5651=PLANE('',#6831);
#5904=ADVANCED_FACE('',(#1188),#1014,.F.);
#5905=ADVANCED_FACE('',(#1189),#1015,.F.);
#5906=ADVANCED_FACE('',(#1190),#1016,.F.);
#5907=ADVANCED_FACE('',(#1191),#1017,.F.);
#5908=ADVANCED_FACE('',(#1192),#1018,.T.);
#5909=ADVANCED_FACE('',(#1193,#569),#5649,.F.);
#5910=ADVANCED_FACE('',(#1194),#1019,.F.);
#5911=ADVANCED_FACE('',(#1195),#1020,.T.);
#5912=ADVANCED_FACE('',(#1196,#570,#571,#572,#573,#574),#5650,.T.);
#5913=ADVANCED_FACE('',(#1197,#575,#576,#577,#578,#579),#5651,.F.);
#6187=CLOSED_SHELL('',(#5904,#5905,#5906,#5907,#5908,#5909,#5910,#5911,
#5912,#5913));
#6807=AXIS2_PLACEMENT_3D('',#9888,#7921,#7922);
#6808=AXIS2_PLACEMENT_3D('',#9889,#7923,#7924);
#6809=AXIS2_PLACEMENT_3D('',#9891,#7925,#7926);
#6810=AXIS2_PLACEMENT_3D('',#9894,#7928,#7929);
#6811=AXIS2_PLACEMENT_3D('',#9895,#7930,#7931);
#6812=AXIS2_PLACEMENT_3D('',#9897,#7932,#7933);
#6813=AXIS2_PLACEMENT_3D('',#9900,#7935,#7936);
#6814=AXIS2_PLACEMENT_3D('',#9901,#7937,#7938);
#6815=AXIS2_PLACEMENT_3D('',#9903,#7939,#7940);
#6816=AXIS2_PLACEMENT_3D('',#9906,#7942,#7943);
#6817=AXIS2_PLACEMENT_3D('',#9907,#7944,#7945);
#6818=AXIS2_PLACEMENT_3D('',#9909,#7946,#7947);
#6819=AXIS2_PLACEMENT_3D('',#9912,#7949,#7950);
#6820=AXIS2_PLACEMENT_3D('',#9913,#7951,#7952);
#6821=AXIS2_PLACEMENT_3D('',#9915,#7953,#7954);
#6822=AXIS2_PLACEMENT_3D('',#9918,#7956,#7957);
#6823=AXIS2_PLACEMENT_3D('',#9919,#7958,#7959);
#6824=AXIS2_PLACEMENT_3D('',#9921,#7960,#7961);
#6825=AXIS2_PLACEMENT_3D('',#9922,#7962,#7963);
#6826=AXIS2_PLACEMENT_3D('',#9924,#7964,#7965);
#6827=AXIS2_PLACEMENT_3D('',#9926,#7967,#7968);
#6828=AXIS2_PLACEMENT_3D('',#9928,#7969,#7970);
#6829=AXIS2_PLACEMENT_3D('',#9931,#7972,#7973);
#6830=AXIS2_PLACEMENT_3D('',#9932,#7974,#7975);
#6831=AXIS2_PLACEMENT_3D('',#9933,#7976,#7977);
#7921=DIRECTION('axis',(0.,0.,1.));
#7922=DIRECTION('refdir',(1.,0.,0.));
#7923=DIRECTION('center_axis',(0.,1.,0.));
#7924=DIRECTION('ref_axis',(1.,0.,0.));
#7925=DIRECTION('center_axis',(0.,1.,0.));
#7926=DIRECTION('ref_axis',(1.,0.,0.));
#7927=DIRECTION('',(0.,1.,0.));
#7928=DIRECTION('center_axis',(0.,-1.,0.));
#7929=DIRECTION('ref_axis',(1.,0.,0.));
#7930=DIRECTION('center_axis',(0.,1.,0.));
#7931=DIRECTION('ref_axis',(1.,0.,0.));
#7932=DIRECTION('center_axis',(0.,1.,0.));
#7933=DIRECTION('ref_axis',(1.,0.,0.));
#7934=DIRECTION('',(0.,1.,0.));
#7935=DIRECTION('center_axis',(0.,-1.,0.));
#7936=DIRECTION('ref_axis',(1.,0.,0.));
#7937=DIRECTION('center_axis',(0.,1.,0.));
#7938=DIRECTION('ref_axis',(1.,0.,0.));
#7939=DIRECTION('center_axis',(0.,1.,0.));
#7940=DIRECTION('ref_axis',(1.,0.,0.));
#7941=DIRECTION('',(0.,1.,0.));
#7942=DIRECTION('center_axis',(0.,-1.,0.));
#7943=DIRECTION('ref_axis',(1.,0.,0.));
#7944=DIRECTION('center_axis',(0.,1.,0.));
#7945=DIRECTION('ref_axis',(1.,0.,0.));
#7946=DIRECTION('center_axis',(0.,1.,0.));
#7947=DIRECTION('ref_axis',(1.,0.,0.));
#7948=DIRECTION('',(0.,1.,0.));
#7949=DIRECTION('center_axis',(0.,-1.,0.));
#7950=DIRECTION('ref_axis',(1.,0.,0.));
#7951=DIRECTION('center_axis',(0.,1.,0.));
#7952=DIRECTION('ref_axis',(1.,0.,0.));
#7953=DIRECTION('center_axis',(0.,1.,0.));
#7954=DIRECTION('ref_axis',(1.,0.,0.));
#7955=DIRECTION('',(0.,-1.,0.));
#7956=DIRECTION('center_axis',(0.,1.,0.));
#7957=DIRECTION('ref_axis',(1.,0.,0.));
#7958=DIRECTION('center_axis',(0.,1.,0.));
#7959=DIRECTION('ref_axis',(1.,0.,0.));
#7960=DIRECTION('center_axis',(0.,-1.,0.));
#7961=DIRECTION('ref_axis',(1.,0.,0.));
#7962=DIRECTION('center_axis',(0.,1.,0.));
#7963=DIRECTION('ref_axis',(1.,0.,0.));
#7964=DIRECTION('center_axis',(0.,-1.,0.));
#7965=DIRECTION('ref_axis',(1.,0.,0.));
#7966=DIRECTION('',(0.,-1.,0.));
#7967=DIRECTION('center_axis',(0.,1.,0.));
#7968=DIRECTION('ref_axis',(1.,0.,0.));
#7969=DIRECTION('center_axis',(0.,1.,0.));
#7970=DIRECTION('ref_axis',(1.,0.,0.));
#7971=DIRECTION('',(0.,-1.,0.));
#7972=DIRECTION('center_axis',(0.,1.,0.));
#7973=DIRECTION('ref_axis',(1.,0.,0.));
#7974=DIRECTION('center_axis',(0.,1.,0.));
#7975=DIRECTION('ref_axis',(1.,0.,0.));
#7976=DIRECTION('center_axis',(0.,1.,0.));
#7977=DIRECTION('ref_axis',(1.,0.,0.));
#9888=CARTESIAN_POINT('',(0.,0.,0.));
#9889=CARTESIAN_POINT('Origin',(-1.4142135623731,3.2,2.58578643762691));
#9890=CARTESIAN_POINT('',(-1.6392135623731,3.3,2.58578643762691));
#9891=CARTESIAN_POINT('Origin',(-1.4142135623731,3.3,2.58578643762691));
#9892=CARTESIAN_POINT('',(-1.6392135623731,3.5,2.58578643762691));
#9893=CARTESIAN_POINT('',(-1.6392135623731,3.2,2.58578643762691));
#9894=CARTESIAN_POINT('Origin',(-1.4142135623731,3.5,2.58578643762691));
#9895=CARTESIAN_POINT('Origin',(-1.41421356237309,3.2,5.41421356237309));
#9896=CARTESIAN_POINT('',(-1.6392135623731,3.3,5.41421356237309));
#9897=CARTESIAN_POINT('Origin',(-1.41421356237309,3.3,5.41421356237309));
#9898=CARTESIAN_POINT('',(-1.6392135623731,3.5,5.41421356237309));
#9899=CARTESIAN_POINT('',(-1.6392135623731,3.2,5.41421356237309));
#9900=CARTESIAN_POINT('Origin',(-1.41421356237309,3.5,5.41421356237309));
#9901=CARTESIAN_POINT('Origin',(1.4142135623731,3.2,5.41421356237309));
#9902=CARTESIAN_POINT('',(1.1892135623731,3.3,5.41421356237309));
#9903=CARTESIAN_POINT('Origin',(1.4142135623731,3.3,5.41421356237309));
#9904=CARTESIAN_POINT('',(1.1892135623731,3.5,5.41421356237309));
#9905=CARTESIAN_POINT('',(1.1892135623731,3.2,5.41421356237309));
#9906=CARTESIAN_POINT('Origin',(1.4142135623731,3.5,5.41421356237309));
#9907=CARTESIAN_POINT('Origin',(1.41421356237309,3.2,2.5857864376269));
#9908=CARTESIAN_POINT('',(1.18921356237309,3.3,2.5857864376269));
#9909=CARTESIAN_POINT('Origin',(1.41421356237309,3.3,2.5857864376269));
#9910=CARTESIAN_POINT('',(1.18921356237309,3.5,2.5857864376269));
#9911=CARTESIAN_POINT('',(1.18921356237309,3.2,2.5857864376269));
#9912=CARTESIAN_POINT('Origin',(1.41421356237309,3.5,2.5857864376269));
#9913=CARTESIAN_POINT('Origin',(0.,3.,4.));
#9914=CARTESIAN_POINT('',(-1.59,3.3,4.));
#9915=CARTESIAN_POINT('Origin',(0.,3.3,4.));
#9916=CARTESIAN_POINT('',(-1.59,3.,4.));
#9917=CARTESIAN_POINT('',(-1.59,3.,4.));
#9918=CARTESIAN_POINT('Origin',(0.,3.,4.));
#9919=CARTESIAN_POINT('Origin',(0.,3.,4.));
#9920=CARTESIAN_POINT('',(-1.005,3.,4.));
#9921=CARTESIAN_POINT('Origin',(0.,3.,4.));
#9922=CARTESIAN_POINT('Origin',(0.,3.3,4.));
#9923=CARTESIAN_POINT('',(-1.005,3.5,4.));
#9924=CARTESIAN_POINT('Origin',(0.,3.5,4.));
#9925=CARTESIAN_POINT('',(-1.005,3.3,4.));
#9926=CARTESIAN_POINT('Origin',(0.,3.3,4.));
#9927=CARTESIAN_POINT('',(-2.4,3.5,4.));
#9928=CARTESIAN_POINT('Origin',(0.,3.5,4.));
#9929=CARTESIAN_POINT('',(-2.4,3.3,4.));
#9930=CARTESIAN_POINT('',(-2.4,3.3,4.));
#9931=CARTESIAN_POINT('Origin',(0.,3.3,4.));
#9932=CARTESIAN_POINT('Origin',(0.,3.5,4.));
#9933=CARTESIAN_POINT('Origin',(0.,3.3,4.));
#12821=UNCERTAINTY_MEASURE_WITH_UNIT(LENGTH_MEASURE(0.001),#12897,
'DISTANCE_ACCURACY_VALUE',
'Maximum model space distance between geometric entities at asserted c
onnectivities');
#12853=UNCERTAINTY_MEASURE_WITH_UNIT(LENGTH_MEASURE(0.001),#12897,
'DISTANCE_ACCURACY_VALUE',
'Maximum model space distance between geometric entities at asserted c
onnectivities');
#12864=(
GEOMETRIC_REPRESENTATION_CONTEXT(3)
GLOBAL_UNCERTAINTY_ASSIGNED_CONTEXT((#12821))
GLOBAL_UNIT_ASSIGNED_CONTEXT((#12897,#12899,#12900))
REPRESENTATION_CONTEXT('','3D')
);
#12896=(
GEOMETRIC_REPRESENTATION_CONTEXT(3)
GLOBAL_UNCERTAINTY_ASSIGNED_CONTEXT((#12853))
GLOBAL_UNIT_ASSIGNED_CONTEXT((#12897,#12899,#12900))
REPRESENTATION_CONTEXT('','3D')
);
#12897=(
LENGTH_UNIT()
NAMED_UNIT(*)
SI_UNIT(.CENTI.,.METRE.)
);
#12899=(
NAMED_UNIT(*)
PLANE_ANGLE_UNIT()
SI_UNIT($,.RADIAN.)
);
#12900=(
NAMED_UNIT(*)
SI_UNIT($,.STERADIAN.)
SOLID_ANGLE_UNIT()
);
#12911=SHAPE_DEFINITION_REPRESENTATION(#12953,#13064);
#12953=PRODUCT_DEFINITION_SHAPE('',$,#13107);
#13064=SHAPE_REPRESENTATION('',(#6807),#12864);
#13096=PRODUCT_DEFINITION_CONTEXT('part definition',#13224,'design');
#13107=PRODUCT_DEFINITION('Bearing cap (3)','Bearing cap (3)',#13149,#13096);
#13149=PRODUCT_DEFINITION_FORMATION('',$,#13236);
#13224=APPLICATION_CONTEXT(
'Core Data for Automotive Mechanical Design Process');
#13225=PRODUCT_CONTEXT('part definition',#13224,'mechanical');
#13236=PRODUCT('Bearing cap (3)','Bearing cap (3)','Bearing cap (3)',(#13225));
#13324=COLOUR_RGB('Grey',0.48,0.52,0.57);
#13325=FILL_AREA_STYLE_COLOUR('',#13324);
#13326=FILL_AREA_STYLE('',(#13325));
#13327=SURFACE_STYLE_FILL_AREA(#13326);
#13328=SURFACE_SIDE_STYLE('',(#13327));
#13329=SURFACE_STYLE_USAGE(.BOTH.,#13328);
#13330=PRESENTATION_STYLE_ASSIGNMENT((#13329));
ENDSEC;
END-ISO-10303-21;
